ISO-10303-21;
HEADER;
FILE_DESCRIPTION (('STEP AP214'),
    '1' );
FILE_NAME ('angular contact ball bearing_68_iso_ISO 15 ABB - 188 - 12,SI,NC,12_68.step',
    '2026-10-08T05:56:58',
    ( '' ),
    ( '' ),
    'SwSTEP 2.0',
    'SolidWorks 2026',
    '' );
FILE_SCHEMA (( 'AUTOMOTIVE_DESIGN' ));
ENDSEC;

DATA;
#11=ADVANCED_FACE ( 'NONE', ( #15453 ), #13841, .T. ) ;
#24=ORIENTED_EDGE ( 'NONE', *, *, #5256, .T. ) ;
#41=DIRECTION ( 'NONE',  ( 0.000000000000000000, 1.224646799147353454E-16, 1.000000000000000000 ) ) ;
#49=DIRECTION ( 'NONE',  ( 0.000000000000000000, 0.000000000000000000, -1.000000000000000000 ) ) ;
#88=DIRECTION ( 'NONE',  ( 0.000000000000000000, 0.000000000000000000, -1.000000000000000000 ) ) ;
#150=STYLED_ITEM ( 'NONE', ( #8512 ), #9431 ) ;
#158=CARTESIAN_POINT ( 'NONE',  ( -0.8944271909999155223, 0.000000000000000000, 0.000000000000000000 ) ) ;
#182=AXIS2_PLACEMENT_3D ( 'NONE', #8021, #14038, #15743 ) ;
#187=DIRECTION ( 'NONE',  ( 0.000000000000000000, 0.000000000000000000, -1.000000000000000000 ) ) ;
#197=EDGE_CURVE ( 'NONE', #5418, #16213, #1053, .T. ) ;
#206=ORIENTED_EDGE ( 'NONE', *, *, #1733, .T. ) ;
#235=CIRCLE ( 'NONE', #5349, 0.1999999999999996503 ) ;
#269=DIRECTION ( 'NONE',  ( 1.000000000000000000, 0.000000000000000000, 0.000000000000000000 ) ) ;
#282=DIRECTION ( 'NONE',  ( 1.000000000000000000, 0.000000000000000000, 0.000000000000000000 ) ) ;
#292=ORIENTED_EDGE ( 'NONE', *, *, #3282, .F. ) ;
#352=ORIENTED_EDGE ( 'NONE', *, *, #18069, .F. ) ;
#396=PRODUCT_DEFINITION ( 'UNKNOWN', '', #3806, #10010 ) ;
#437=VECTOR ( 'NONE', #17794, 1000.000000000000000 ) ;
#444=CARTESIAN_POINT ( 'NONE',  ( -1.799999999999999600, 9.797174393178827630E-16, 8.000000000000000000 ) ) ;
#461=( GEOMETRIC_REPRESENTATION_CONTEXT ( 3 ) GLOBAL_UNCERTAINTY_ASSIGNED_CONTEXT ( ( #5578 ) ) GLOBAL_UNIT_ASSIGNED_CONTEXT ( ( #6065, #13682, #1180 ) ) REPRESENTATION_CONTEXT ( 'NONE', 'WORKASPACE' ) );
#492=ADVANCED_FACE ( 'NONE', ( #12129 ), #16089, .T. ) ;
#517=DIRECTION ( 'NONE',  ( 0.000000000000000000, 0.000000000000000000, -1.000000000000000000 ) ) ;
#531=EDGE_CURVE ( 'NONE', #12054, #4447, #7429, .T. ) ;
#576=CYLINDRICAL_SURFACE ( 'NONE', #10772, 4.824999999999999289 ) ;
#599=CARTESIAN_POINT ( 'NONE',  ( 0.2436698586202201144, 0.000000000000000000, 0.000000000000000000 ) ) ;
#635=EDGE_LOOP ( 'NONE', ( #13880, #12061, #1911, #8139 ) ) ;
#639=VERTEX_POINT ( 'NONE', #10529 ) ;
#641=CARTESIAN_POINT ( 'NONE',  ( 1.800000000000000044, 0.000000000000000000, 0.000000000000000000 ) ) ;
#715=CIRCLE ( 'NONE', #14455, 1.199999999999999734 ) ;
#755=FACE_OUTER_BOUND ( 'NONE', #6243, .T. ) ;
#763=DIRECTION ( 'NONE',  ( 0.000000000000000000, -1.000000000000000000, 0.000000000000000000 ) ) ;
#783=EDGE_CURVE ( 'NONE', #14953, #18565, #5859, .T. ) ;
#801=CYLINDRICAL_SURFACE ( 'NONE', #8075, 8.000000000000000000 ) ;
#815=DIRECTION ( 'NONE',  ( -1.000000000000000000, 0.000000000000000000, -0.000000000000000000 ) ) ;
#821=DIRECTION ( 'NONE',  ( 1.000000000000000000, 0.000000000000000000, 0.000000000000000000 ) ) ;
#825=CARTESIAN_POINT ( 'NONE',  ( -2.000000000000001776, 0.000000000000000000, 0.000000000000000000 ) ) ;
#826=ORIENTED_EDGE ( 'NONE', *, *, #7927, .F. ) ;
#851=DIRECTION ( 'NONE',  ( 1.000000000000000000, 0.000000000000000000, 0.000000000000000000 ) ) ;
#876=ORIENTED_EDGE ( 'NONE', *, *, #5256, .F. ) ;
#884=APPLICATION_CONTEXT ( 'automotive_design' ) ;
#889=SURFACE_STYLE_FILL_AREA ( #8496 ) ;
#926=ORIENTED_EDGE ( 'NONE', *, *, #17404, .F. ) ;
#986=DIRECTION ( 'NONE',  ( 0.000000000000000000, 1.000000000000000000, -1.224646799147353207E-16 ) ) ;
#1004=DIRECTION ( 'NONE',  ( 0.000000000000000000, 0.000000000000000000, -1.000000000000000000 ) ) ;
#1035=ORIENTED_EDGE ( 'NONE', *, *, #8366, .F. ) ;
#1053=CIRCLE ( 'NONE', #13502, 1.199999999999999734 ) ;
#1091=STYLED_ITEM ( 'NONE', ( #13477 ), #4233 ) ;
#1097=ADVANCED_FACE ( 'NONE', ( #9600 ), #1889, .F. ) ;
#1107=VERTEX_POINT ( 'NONE', #4987 ) ;
#1137=VECTOR ( 'NONE', #2464, 1000.000000000000000 ) ;
#1164=CIRCLE ( 'NONE', #6254, 5.200000000000000178 ) ;
#1180=( NAMED_UNIT ( * ) SI_UNIT ( $, .STERADIAN. ) SOLID_ANGLE_UNIT ( ) );
#1197=FACE_OUTER_BOUND ( 'NONE', #635, .T. ) ;
#1238=DIRECTION ( 'NONE',  ( 1.000000000000000000, 0.000000000000000000, 0.000000000000000000 ) ) ;
#1255=EDGE_CURVE ( 'NONE', #12054, #5418, #5238, .T. ) ;
#1258=EDGE_CURVE ( 'NONE', #13729, #18135, #15151, .T. ) ;
#1277=TOROIDAL_SURFACE ( 'NONE', #5732, 6.000000000000000000, 1.199999999999999956 ) ;
#1342=EDGE_CURVE ( 'NONE', #7744, #1107, #11879, .T. ) ;
#1367=DIRECTION ( 'NONE',  ( 0.000000000000000000, 0.000000000000000000, -1.000000000000000000 ) ) ;
#1373=ORIENTED_EDGE ( 'NONE', *, *, #17144, .T. ) ;
#1387=AXIS2_PLACEMENT_3D ( 'NONE', #13826, #11927, #6109 ) ;
#1390=AXIS2_PLACEMENT_3D ( 'NONE', #11103, #17206, #15704 ) ;
#1429=VECTOR ( 'NONE', #11222, 1000.000000000000000 ) ;
#1478=SURFACE_STYLE_USAGE ( .BOTH. , #19182 ) ;
#1480=ORIENTED_EDGE ( 'NONE', *, *, #19044, .F. ) ;
#1552=CARTESIAN_POINT ( 'NONE',  ( 0.8944271909999176318, 0.000000000000000000, 6.799999999999998046 ) ) ;
#1558=ORIENTED_EDGE ( 'NONE', *, *, #7927, .T. ) ;
#1568=FACE_OUTER_BOUND ( 'NONE', #7860, .T. ) ;
#1573=VERTEX_POINT ( 'NONE', #8930 ) ;
#1582=DIRECTION ( 'NONE',  ( 0.000000000000000000, 0.000000000000000000, -1.000000000000000000 ) ) ;
#1583=DIRECTION ( 'NONE',  ( 0.000000000000000000, 0.000000000000000000, -1.000000000000000000 ) ) ;
#1600=ORIENTED_EDGE ( 'NONE', *, *, #19608, .F. ) ;
#1607=AXIS2_PLACEMENT_3D ( 'NONE', #3039, #16766, #18257 ) ;
#1640=ADVANCED_FACE ( 'NONE', ( #3219, #15338 ), #18427, .T. ) ;
#1648=DIRECTION ( 'NONE',  ( 0.000000000000000000, 0.000000000000000000, -1.000000000000000000 ) ) ;
#1689=TOROIDAL_SURFACE ( 'NONE', #18618, 4.200000000000000178, 0.1999999999999998723 ) ;
#1715=ORIENTED_EDGE ( 'NONE', *, *, #15941, .T. ) ;
#1725=DIRECTION ( 'NONE',  ( 1.000000000000000000, 0.000000000000000000, 0.000000000000000000 ) ) ;
#1733=EDGE_CURVE ( 'NONE', #12398, #5418, #9835, .T. ) ;
#1767=DIRECTION ( 'NONE',  ( 0.000000000000000000, 0.000000000000000000, -1.000000000000000000 ) ) ;
#1795=CARTESIAN_POINT ( 'NONE',  ( 2.000000000000001776, 0.000000000000000000, -6.799999999999998934 ) ) ;
#1823=EDGE_LOOP ( 'NONE', ( #5096, #15538, #17838, #15877 ) ) ;
#1889=CYLINDRICAL_SURFACE ( 'NONE', #16410, 6.799999999999998046 ) ;
#1911=ORIENTED_EDGE ( 'NONE', *, *, #5430, .F. ) ;
#1953=CARTESIAN_POINT ( 'NONE',  ( -2.000000000000000888, 0.000000000000000000, -4.200000000000000178 ) ) ;
#1991=DIRECTION ( 'NONE',  ( -1.000000000000000000, -0.000000000000000000, -0.000000000000000000 ) ) ;
#1997=AXIS2_PLACEMENT_3D ( 'NONE', #6531, #3544, #49 ) ;
#1998=DIRECTION ( 'NONE',  ( 0.000000000000000000, 0.000000000000000000, -1.000000000000000000 ) ) ;
#2017=EDGE_CURVE ( 'NONE', #12768, #13068, #7816, .T. ) ;
#2021=CARTESIAN_POINT ( 'NONE',  ( -2.000000000000001776, 0.000000000000000000, 0.000000000000000000 ) ) ;
#2110=VERTEX_POINT ( 'NONE', #1795 ) ;
#2118=CARTESIAN_POINT ( 'NONE',  ( 0.2436698586202201144, 0.000000000000000000, 4.824999999999999289 ) ) ;
#2167=CARTESIAN_POINT ( 'NONE',  ( 1.799999999999999600, 0.000000000000000000, 0.000000000000000000 ) ) ;
#2170=AXIS2_PLACEMENT_3D ( 'NONE', #8194, #8589, #12800 ) ;
#2207=DIRECTION ( 'NONE',  ( 0.000000000000000000, 0.000000000000000000, -1.000000000000000000 ) ) ;
#2234=CYLINDRICAL_SURFACE ( 'NONE', #8483, 6.799999999999998046 ) ;
#2239=VERTEX_POINT ( 'NONE', #5288 ) ;
#2273=EDGE_LOOP ( 'NONE', ( #10672, #6690, #8318, #4678 ) ) ;
#2300=( LENGTH_UNIT ( ) NAMED_UNIT ( * ) SI_UNIT ( .MILLI., .METRE. ) );
#2301=FACE_OUTER_BOUND ( 'NONE', #3565, .T. ) ;
#2338=CARTESIAN_POINT ( 'NONE',  ( -20.63749999999999929, 6.368163355566236381E-16, 5.200000000000000178 ) ) ;
#2343=CARTESIAN_POINT ( 'NONE',  ( -1.799999999999999600, 0.000000000000000000, 0.000000000000000000 ) ) ;
#2453=ORIENTED_EDGE ( 'NONE', *, *, #10690, .F. ) ;
#2459=ORIENTED_EDGE ( 'NONE', *, *, #10655, .T. ) ;
#2464=DIRECTION ( 'NONE',  ( 1.000000000000000000, 0.000000000000000000, 0.000000000000000000 ) ) ;
#2471=ADVANCED_FACE ( 'NONE', ( #11882, #12088 ), #5766, .T. ) ;
#2512=CARTESIAN_POINT ( 'NONE',  ( 0.2436698586202201144, 0.000000000000000000, 0.000000000000000000 ) ) ;
#2531=ORIENTED_EDGE ( 'NONE', *, *, #12349, .F. ) ;
#2534=FACE_OUTER_BOUND ( 'NONE', #18518, .T. ) ;
#2562=CIRCLE ( 'NONE', #17287, 4.200000000000000178 ) ;
#2564=DIRECTION ( 'NONE',  ( 0.000000000000000000, -1.224646799147353207E-16, 1.000000000000000000 ) ) ;
#2576=AXIS2_PLACEMENT_3D ( 'NONE', #10946, #14446, #8238 ) ;
#2589=ADVANCED_FACE ( 'NONE', ( #9281 ), #1689, .T. ) ;
#2622=CARTESIAN_POINT ( 'NONE',  ( -20.63749999999999929, 0.000000000000000000, 0.000000000000000000 ) ) ;
#2626=CARTESIAN_POINT ( 'NONE',  ( 1.799999999999999600, 0.000000000000000000, -8.000000000000000000 ) ) ;
#2636=CIRCLE ( 'NONE', #14472, 1.199999999999999734 ) ;
#2663=DIRECTION ( 'NONE',  ( 0.000000000000000000, 0.000000000000000000, -1.000000000000000000 ) ) ;
#2665=CARTESIAN_POINT ( 'NONE',  ( 1.800000000000000044, 0.000000000000000000, 0.000000000000000000 ) ) ;
#2707=AXIS2_PLACEMENT_3D ( 'NONE', #7173, #4100, #13493 ) ;
#2741=FACE_OUTER_BOUND ( 'NONE', #14563, .T. ) ;
#2815=CARTESIAN_POINT ( 'NONE',  ( 1.799999999999999600, 0.000000000000000000, 0.000000000000000000 ) ) ;
#2834=EDGE_CURVE ( 'NONE', #2110, #17016, #10627, .T. ) ;
#2843=DIRECTION ( 'NONE',  ( -1.000000000000000000, -0.000000000000000000, -0.000000000000000000 ) ) ;
#2858=CARTESIAN_POINT ( 'NONE',  ( -1.800000000000000488, 5.143516556418882928E-16, 4.200000000000000178 ) ) ;
#2866=DIRECTION ( 'NONE',  ( 1.000000000000000000, 0.000000000000000000, 0.000000000000000000 ) ) ;
#2879=DIRECTION ( 'NONE',  ( 0.000000000000000000, 0.000000000000000000, -1.000000000000000000 ) ) ;
#2892=DIRECTION ( 'NONE',  ( 1.000000000000000000, 0.000000000000000000, 0.000000000000000000 ) ) ;
#2899=DIRECTION ( 'NONE',  ( 1.000000000000000000, 0.000000000000000000, 0.000000000000000000 ) ) ;
#2983=DIRECTION ( 'NONE',  ( 0.000000000000000000, 0.000000000000000000, -1.000000000000000000 ) ) ;
#3018=AXIS2_PLACEMENT_3D ( 'NONE', #16840, #1725, #7815 ) ;
#3039=CARTESIAN_POINT ( 'NONE',  ( -1.800000000000000488, 0.000000000000000000, 0.000000000000000000 ) ) ;
#3061=ORIENTED_EDGE ( 'NONE', *, *, #3062, .T. ) ;
#3062=EDGE_CURVE ( 'NONE', #7744, #1573, #11925, .T. ) ;
#3073=VERTEX_POINT ( 'NONE', #2626 ) ;
#3091=ORIENTED_EDGE ( 'NONE', *, *, #7862, .F. ) ;
#3108=EDGE_CURVE ( 'NONE', #6978, #16213, #14302, .T. ) ;
#3114=AXIS2_PLACEMENT_3D ( 'NONE', #17305, #7895, #1998 ) ;
#3162=DIRECTION ( 'NONE',  ( 0.000000000000000000, -1.000000000000000000, 0.000000000000000000 ) ) ;
#3177=ADVANCED_FACE ( 'NONE', ( #7991, #6478 ), #12612, .T. ) ;
#3205=ORIENTED_EDGE ( 'NONE', *, *, #12349, .T. ) ;
#3216=EDGE_CURVE ( 'NONE', #17337, #8711, #17047, .T. ) ;
#3217=ADVANCED_FACE ( 'NONE', ( #13003 ), #801, .T. ) ;
#3219=FACE_OUTER_BOUND ( 'NONE', #9733, .T. ) ;
#3240=EDGE_LOOP ( 'NONE', ( #6363, #18871, #3205, #14448 ) ) ;
#3269=ORIENTED_EDGE ( 'NONE', *, *, #17032, .T. ) ;
#3282=EDGE_CURVE ( 'NONE', #2239, #12054, #16394, .T. ) ;
#3359=EDGE_LOOP ( 'NONE', ( #17713, #7279 ) ) ;
#3400=CARTESIAN_POINT ( 'NONE',  ( -1.799999999999999600, 0.000000000000000000, 0.000000000000000000 ) ) ;
#3457=ORIENTED_EDGE ( 'NONE', *, *, #6080, .F. ) ;
#3473=ORIENTED_EDGE ( 'NONE', *, *, #1258, .T. ) ;
#3482=CYLINDRICAL_SURFACE ( 'NONE', #10128, 7.174999999999998934 ) ;
#3530=ORIENTED_EDGE ( 'NONE', *, *, #17996, .F. ) ;
#3542=ORIENTED_EDGE ( 'NONE', *, *, #5489, .F. ) ;
#3544=DIRECTION ( 'NONE',  ( 1.000000000000000000, 0.000000000000000000, 0.000000000000000000 ) ) ;
#3565=EDGE_LOOP ( 'NONE', ( #15916, #826 ) ) ;
#3634=DIRECTION ( 'NONE',  ( 1.000000000000000000, 0.000000000000000000, 0.000000000000000000 ) ) ;
#3652=CIRCLE ( 'NONE', #17105, 4.000000000000000000 ) ;
#3668=ORIENTED_EDGE ( 'NONE', *, *, #2017, .F. ) ;
#3781=CARTESIAN_POINT ( 'NONE',  ( -20.63749999999999929, 0.000000000000000000, -4.824999999999999289 ) ) ;
#3786=( LENGTH_UNIT ( ) NAMED_UNIT ( * ) SI_UNIT ( .MILLI., .METRE. ) );
#3806=PRODUCT_DEFINITION_FORMATION_WITH_SPECIFIED_SOURCE ( 'ANY', '', #4114, .NOT_KNOWN. ) ;
#3844=CARTESIAN_POINT ( 'NONE',  ( -0.8944271909999155223, 0.000000000000000000, -5.200000000000000178 ) ) ;
#3878=CARTESIAN_POINT ( 'NONE',  ( -0.2436698586202288019, 0.000000000000000000, 0.000000000000000000 ) ) ;
#3886=CYLINDRICAL_SURFACE ( 'NONE', #2170, 4.824999999999999289 ) ;
#3895=ORIENTED_EDGE ( 'NONE', *, *, #1258, .F. ) ;
#3919=EDGE_CURVE ( 'NONE', #18537, #6978, #11105, .T. ) ;
#3933=DIRECTION ( 'NONE',  ( 1.000000000000000000, 0.000000000000000000, 0.000000000000000000 ) ) ;
#3964=TOROIDAL_SURFACE ( 'NONE', #19289, 7.800000000000000711, 0.1999999999999998723 ) ;
#3984=DIRECTION ( 'NONE',  ( 0.000000000000000000, 0.000000000000000000, -1.000000000000000000 ) ) ;
#4001=SURFACE_STYLE_USAGE ( .BOTH. , #16012 ) ;
#4003=DIRECTION ( 'NONE',  ( 1.000000000000000000, 0.000000000000000000, 0.000000000000000000 ) ) ;
#4006=DIRECTION ( 'NONE',  ( 0.000000000000000000, 0.000000000000000000, 1.000000000000000000 ) ) ;
#4032=AXIS2_PLACEMENT_3D ( 'NONE', #18818, #821, #2207 ) ;
#4039=FACE_OUTER_BOUND ( 'NONE', #14358, .T. ) ;
#4042=DIRECTION ( 'NONE',  ( 0.000000000000000000, 0.000000000000000000, -1.000000000000000000 ) ) ;
#4053=AXIS2_PLACEMENT_3D ( 'NONE', #12912, #13792, #88 ) ;
#4075=VECTOR ( 'NONE', #15411, 1000.000000000000000 ) ;
#4079=EDGE_CURVE ( 'NONE', #12768, #6633, #235, .T. ) ;
#4100=DIRECTION ( 'NONE',  ( 1.000000000000000000, 0.000000000000000000, 0.000000000000000000 ) ) ;
#4104=DIRECTION ( 'NONE',  ( 1.000000000000000000, 0.000000000000000000, 0.000000000000000000 ) ) ;
#4114=PRODUCT ( 'angular contact ball bearing_68_iso_ISO 15 ABB - 188 - 12,SI,NC,12_68', 'angular contact ball bearing_68_iso_ISO 15 ABB - 188 - 12,SI,NC,12_68', '', ( #15657 ) ) ;
#4162=TOROIDAL_SURFACE ( 'NONE', #1607, 4.200000000000000178, 0.1999999999999998723 ) ;
#4171=ORIENTED_EDGE ( 'NONE', *, *, #11692, .T. ) ;
#4185=DIRECTION ( 'NONE',  ( 1.000000000000000000, 0.000000000000000000, 0.000000000000000000 ) ) ;
#4233=ADVANCED_BREP_SHAPE_REPRESENTATION ( '', ( #9431, #16724 ), #16113 ) ;
#4250=ADVANCED_FACE ( 'NONE', ( #2534 ), #5347, .F. ) ;
#4255=VECTOR ( 'NONE', #15804, 1000.000000000000000 ) ;
#4289=AXIS2_PLACEMENT_3D ( 'NONE', #13858, #17157, #5134 ) ;
#4301=MECHANICAL_DESIGN_GEOMETRIC_PRESENTATION_REPRESENTATION('',(#150),#15492);
#4389=DIRECTION ( 'NONE',  ( 1.000000000000000000, 0.000000000000000000, 0.000000000000000000 ) ) ;
#4421=ORIENTED_EDGE ( 'NONE', *, *, #8366, .T. ) ;
#4447=VERTEX_POINT ( 'NONE', #8229 ) ;
#4475=DIRECTION ( 'NONE',  ( 0.000000000000000000, 0.000000000000000000, -1.000000000000000000 ) ) ;
#4678=ORIENTED_EDGE ( 'NONE', *, *, #10655, .F. ) ;
#4687=DIRECTION ( 'NONE',  ( 0.000000000000000000, -1.000000000000000000, 0.000000000000000000 ) ) ;
#4744=ORIENTED_EDGE ( 'NONE', *, *, #531, .F. ) ;
#4746=ORIENTED_EDGE ( 'NONE', *, *, #14634, .F. ) ;
#4772=CARTESIAN_POINT ( 'NONE',  ( 1.800000000000000488, 0.000000000000000000, 0.000000000000000000 ) ) ;
#4825=DIRECTION ( 'NONE',  ( 0.000000000000000000, 0.000000000000000000, -1.000000000000000000 ) ) ;
#4918=COLOUR_RGB ( '', 0.31764706, 0.68627451, 0.89019608) ;
#4921=CARTESIAN_POINT ( 'NONE',  ( -20.63749999999999574, 0.000000000000000000, -7.174999999999998934 ) ) ;
#4935=EDGE_CURVE ( 'NONE', #8711, #13634, #18165, .T. ) ;
#4948=ORIENTED_EDGE ( 'NONE', *, *, #7884, .T. ) ;
#4969=DIRECTION ( 'NONE',  ( 0.000000000000000000, 0.000000000000000000, -1.000000000000000000 ) ) ;
#4987=CARTESIAN_POINT ( 'NONE',  ( 1.799999999999999600, 5.021051876504148371E-16, 4.000000000000000000 ) ) ;
#5028=CARTESIAN_POINT ( 'NONE',  ( -20.63749999999999929, 0.000000000000000000, 0.000000000000000000 ) ) ;
#5096=ORIENTED_EDGE ( 'NONE', *, *, #197, .F. ) ;
#5122=ORIENTED_EDGE ( 'NONE', *, *, #9921, .F. ) ;
#5134=DIRECTION ( 'NONE',  ( 0.000000000000000000, 0.000000000000000000, -1.000000000000000000 ) ) ;
#5225=AXIS2_PLACEMENT_3D ( 'NONE', #12918, #4104, #17615 ) ;
#5237=CLOSED_SHELL ( 'NONE', ( #14485, #3217, #14989, #4250, #14217, #18580, #18570, #13866, #10815, #9582, #12509, #19633, #16393, #11700, #8046, #1640, #2589, #16211, #17219, #3177, #492, #1097, #6247, #19199, #8587, #11, #2471, #17465 ) ) ;
#5238=CIRCLE ( 'NONE', #18034, 7.174999999999998934 ) ;
#5256=EDGE_CURVE ( 'NONE', #8384, #639, #7517, .T. ) ;
#5265=AXIS2_PLACEMENT_3D ( 'NONE', #15011, #2892, #7380 ) ;
#5273=ORIENTED_EDGE ( 'NONE', *, *, #3062, .F. ) ;
#5283=DIRECTION ( 'NONE',  ( -1.000000000000000000, -0.000000000000000000, -0.000000000000000000 ) ) ;
#5288=CARTESIAN_POINT ( 'NONE',  ( -2.000000000000001776, 8.786840783882259896E-16, 7.175000000000000711 ) ) ;
#5308=FACE_OUTER_BOUND ( 'NONE', #14019, .T. ) ;
#5347=CYLINDRICAL_SURFACE ( 'NONE', #12067, 7.174999999999998934 ) ;
#5349=AXIS2_PLACEMENT_3D ( 'NONE', #11163, #763, #18658 ) ;
#5374=DIRECTION ( 'NONE',  ( 1.000000000000000000, 0.000000000000000000, 0.000000000000000000 ) ) ;
#5381=( NAMED_UNIT ( * ) SI_UNIT ( $, .STERADIAN. ) SOLID_ANGLE_UNIT ( ) );
#5392=EDGE_CURVE ( 'NONE', #18565, #14953, #17440, .T. ) ;
#5400=FILL_AREA_STYLE_COLOUR ( '', #8776 ) ;
#5418=VERTEX_POINT ( 'NONE', #11439 ) ;
#5430=EDGE_CURVE ( 'NONE', #16213, #4447, #18078, .T. ) ;
#5431=CIRCLE ( 'NONE', #19170, 7.174999999999999822 ) ;
#5438=DIRECTION ( 'NONE',  ( 0.000000000000000000, 0.000000000000000000, -1.000000000000000000 ) ) ;
#5489=EDGE_CURVE ( 'NONE', #19760, #11964, #14876, .T. ) ;
#5578=UNCERTAINTY_MEASURE_WITH_UNIT (LENGTH_MEASURE( 1.000000000000000082E-05 ), #6065, 'distance_accuracy_value', 'NONE');
#5590=DIRECTION ( 'NONE',  ( -1.000000000000000000, -0.000000000000000000, -0.000000000000000000 ) ) ;
#5620=ORIENTED_EDGE ( 'NONE', *, *, #11910, .T. ) ;
#5624=DIRECTION ( 'NONE',  ( 1.000000000000000000, 0.000000000000000000, 0.000000000000000000 ) ) ;
#5706=DIRECTION ( 'NONE',  ( 0.000000000000000000, 0.000000000000000000, 1.000000000000000000 ) ) ;
#5732=AXIS2_PLACEMENT_3D ( 'NONE', #17332, #18829, #10934 ) ;
#5750=CIRCLE ( 'NONE', #11210, 4.824999999999999289 ) ;
#5766=PLANE ( 'NONE',  #15726 ) ;
#5767=ORIENTED_EDGE ( 'NONE', *, *, #5430, .T. ) ;
#5806=EDGE_LOOP ( 'NONE', ( #16165, #15552, #17610, #2531 ) ) ;
#5859=CIRCLE ( 'NONE', #5225, 6.799999999999998046 ) ;
#5864=CARTESIAN_POINT ( 'NONE',  ( -1.800000000000000044, 0.000000000000000000, 0.000000000000000000 ) ) ;
#5931=CIRCLE ( 'NONE', #7852, 4.000000000000000000 ) ;
#5997=LINE ( 'NONE', #17823, #6430 ) ;
#6003=CIRCLE ( 'NONE', #8570, 5.200000000000000178 ) ;
#6027=DIRECTION ( 'NONE',  ( 1.000000000000000000, 0.000000000000000000, 0.000000000000000000 ) ) ;
#6065=( LENGTH_UNIT ( ) NAMED_UNIT ( * ) SI_UNIT ( .MILLI., .METRE. ) );
#6080=EDGE_CURVE ( 'NONE', #13634, #8711, #12352, .T. ) ;
#6106=AXIS2_PLACEMENT_3D ( 'NONE', #11383, #6953, #14587 ) ;
#6109=DIRECTION ( 'NONE',  ( 0.000000000000000000, 0.000000000000000000, -1.000000000000000000 ) ) ;
#6120=CARTESIAN_POINT ( 'NONE',  ( -2.000000000000001776, 9.674709713264090115E-16, 7.800000000000000711 ) ) ;
#6123=CIRCLE ( 'NONE', #11238, 7.174999999999998934 ) ;
#6129=EDGE_CURVE ( 'NONE', #11459, #9163, #6584, .T. ) ;
#6189=MECHANICAL_DESIGN_GEOMETRIC_PRESENTATION_REPRESENTATION('',(#1091),#461);
#6209=ORIENTED_EDGE ( 'NONE', *, *, #1255, .F. ) ;
#6230=DIRECTION ( 'NONE',  ( 1.000000000000000000, 0.000000000000000000, 0.000000000000000000 ) ) ;
#6243=EDGE_LOOP ( 'NONE', ( #7704, #4746, #1373, #11983 ) ) ;
#6247=ADVANCED_FACE ( 'NONE', ( #14082 ), #3482, .F. ) ;
#6254=AXIS2_PLACEMENT_3D ( 'NONE', #16936, #18524, #14119 ) ;
#6363=ORIENTED_EDGE ( 'NONE', *, *, #17641, .F. ) ;
#6411=CARTESIAN_POINT ( 'NONE',  ( -0.8944271909999155223, 0.000000000000000000, 0.000000000000000000 ) ) ;
#6430=VECTOR ( 'NONE', #2899, 1000.000000000000000 ) ;
#6443=CARTESIAN_POINT ( 'NONE',  ( 0.000000000000000000, 0.000000000000000000, 6.000000000000000000 ) ) ;
#6448=ORIENTED_EDGE ( 'NONE', *, *, #12944, .F. ) ;
#6478=FACE_OUTER_BOUND ( 'NONE', #14255, .T. ) ;
#6531=CARTESIAN_POINT ( 'NONE',  ( 2.000000000000001776, 0.000000000000000000, 0.000000000000000000 ) ) ;
#6584=CIRCLE ( 'NONE', #17785, 0.1999999999999996503 ) ;
#6633=VERTEX_POINT ( 'NONE', #14847 ) ;
#6690=ORIENTED_EDGE ( 'NONE', *, *, #17404, .T. ) ;
#6691=SURFACE_STYLE_FILL_AREA ( #18909 ) ;
#6702=ORIENTED_EDGE ( 'NONE', *, *, #19012, .T. ) ;
#6716=DIRECTION ( 'NONE',  ( 0.000000000000000000, 0.000000000000000000, -1.000000000000000000 ) ) ;
#6738=ORIENTED_EDGE ( 'NONE', *, *, #3919, .T. ) ;
#6776=DIRECTION ( 'NONE',  ( 0.000000000000000000, 0.000000000000000000, 1.000000000000000000 ) ) ;
#6921=FACE_OUTER_BOUND ( 'NONE', #5806, .T. ) ;
#6934=AXIS2_PLACEMENT_3D ( 'NONE', #2021, #15437, #4825 ) ;
#6953=DIRECTION ( 'NONE',  ( 1.000000000000000000, 0.000000000000000000, 0.000000000000000000 ) ) ;
#6978=VERTEX_POINT ( 'NONE', #17726 ) ;
#6979=EDGE_CURVE ( 'NONE', #639, #3073, #5997, .T. ) ;
#7052=CIRCLE ( 'NONE', #6106, 4.200000000000000178 ) ;
#7065=DIRECTION ( 'NONE',  ( 0.000000000000000000, 0.000000000000000000, -1.000000000000000000 ) ) ;
#7119=CARTESIAN_POINT ( 'NONE',  ( -20.63749999999999929, 0.000000000000000000, 0.000000000000000000 ) ) ;
#7159=( NAMED_UNIT ( * ) PLANE_ANGLE_UNIT ( ) SI_UNIT ( $, .RADIAN. ) );
#7161=EDGE_LOOP ( 'NONE', ( #11067, #14422, #19470, #18648 ) ) ;
#7173=CARTESIAN_POINT ( 'NONE',  ( -20.63749999999999929, 0.000000000000000000, 0.000000000000000000 ) ) ;
#7213=CYLINDRICAL_SURFACE ( 'NONE', #12450, 4.000000000000000000 ) ;
#7217=CARTESIAN_POINT ( 'NONE',  ( -20.63749999999999574, 0.000000000000000000, 0.000000000000000000 ) ) ;
#7257=EDGE_LOOP ( 'NONE', ( #10426, #10956, #5767, #4744 ) ) ;
#7279=ORIENTED_EDGE ( 'NONE', *, *, #15691, .T. ) ;
#7284=LINE ( 'NONE', #13508, #4075 ) ;
#7353=CARTESIAN_POINT ( 'NONE',  ( -20.63749999999999929, 4.898587196589412829E-16, 4.000000000000000000 ) ) ;
#7361=UNCERTAINTY_MEASURE_WITH_UNIT (LENGTH_MEASURE( 1.000000000000000082E-05 ), #2300, 'distance_accuracy_value', 'NONE');
#7380=DIRECTION ( 'NONE',  ( 0.000000000000000000, 0.000000000000000000, -1.000000000000000000 ) ) ;
#7420=CARTESIAN_POINT ( 'NONE',  ( 2.000000000000001776, 0.000000000000000000, 0.000000000000000000 ) ) ;
#7428=CARTESIAN_POINT ( 'NONE',  ( 1.800000000000000488, 5.143516556418882928E-16, 4.200000000000000178 ) ) ;
#7429=CIRCLE ( 'NONE', #1387, 1.199999999999999734 ) ;
#7517=CIRCLE ( 'NONE', #11049, 0.1999999999999996503 ) ;
#7535=CARTESIAN_POINT ( 'NONE',  ( 1.799999999999999600, 0.000000000000000000, 0.000000000000000000 ) ) ;
#7569=DIRECTION ( 'NONE',  ( 0.000000000000000000, 0.000000000000000000, -1.000000000000000000 ) ) ;
#7599=EDGE_CURVE ( 'NONE', #8384, #13729, #12544, .T. ) ;
#7605=AXIS2_PLACEMENT_3D ( 'NONE', #2167, #12978, #17677 ) ;
#7704=ORIENTED_EDGE ( 'NONE', *, *, #1342, .F. ) ;
#7744=VERTEX_POINT ( 'NONE', #8274 ) ;
#7775=DIRECTION ( 'NONE',  ( 1.000000000000000000, 0.000000000000000000, 0.000000000000000000 ) ) ;
#7796=TOROIDAL_SURFACE ( 'NONE', #4289, 7.800000000000000711, 0.1999999999999998723 ) ;
#7815=DIRECTION ( 'NONE',  ( 0.000000000000000000, 0.000000000000000000, -1.000000000000000000 ) ) ;
#7816=CIRCLE ( 'NONE', #5265, 4.200000000000000178 ) ;
#7852=AXIS2_PLACEMENT_3D ( 'NONE', #2815, #15033, #12034 ) ;
#7860=EDGE_LOOP ( 'NONE', ( #3895, #1558, #24, #8566 ) ) ;
#7862=EDGE_CURVE ( 'NONE', #1573, #9163, #7052, .T. ) ;
#7884=EDGE_CURVE ( 'NONE', #18970, #9059, #9692, .T. ) ;
#7895=DIRECTION ( 'NONE',  ( 1.000000000000000000, 0.000000000000000000, 0.000000000000000000 ) ) ;
#7902=ORIENTED_EDGE ( 'NONE', *, *, #783, .T. ) ;
#7921=AXIS2_PLACEMENT_3D ( 'NONE', #3400, #9511, #12703 ) ;
#7927=EDGE_CURVE ( 'NONE', #13729, #8384, #10641, .T. ) ;
#7991=FACE_BOUND ( 'NONE', #10482, .T. ) ;
#8021=CARTESIAN_POINT ( 'NONE',  ( 0.8944271909999177428, 0.000000000000000000, 0.000000000000000000 ) ) ;
#8027=CARTESIAN_POINT ( 'NONE',  ( -20.63749999999999929, 5.908920805885978590E-16, 4.824999999999999289 ) ) ;
#8046=ADVANCED_FACE ( 'NONE', ( #13942 ), #17142, .T. ) ;
#8053=FACE_OUTER_BOUND ( 'NONE', #18288, .T. ) ;
#8067=AXIS2_PLACEMENT_3D ( 'NONE', #5864, #16383, #2663 ) ;
#8075=AXIS2_PLACEMENT_3D ( 'NONE', #17598, #4185, #7065 ) ;
#8097=CARTESIAN_POINT ( 'NONE',  ( 2.000000000000001776, 0.000000000000000000, -7.800000000000000711 ) ) ;
#8112=EDGE_LOOP ( 'NONE', ( #4171, #15424, #3457, #14149 ) ) ;
#8130=DIRECTION ( 'NONE',  ( 1.000000000000000000, 0.000000000000000000, 0.000000000000000000 ) ) ;
#8139=ORIENTED_EDGE ( 'NONE', *, *, #3108, .F. ) ;
#8194=CARTESIAN_POINT ( 'NONE',  ( -20.63749999999999929, 0.000000000000000000, 0.000000000000000000 ) ) ;
#8229=CARTESIAN_POINT ( 'NONE',  ( -0.8944271909999155223, 6.368163355566236381E-16, 5.200000000000000178 ) ) ;
#8234=ORIENTED_EDGE ( 'NONE', *, *, #4935, .T. ) ;
#8238=DIRECTION ( 'NONE',  ( 0.000000000000000000, 0.000000000000000000, -1.000000000000000000 ) ) ;
#8274=CARTESIAN_POINT ( 'NONE',  ( -1.799999999999999600, 4.898587196589412829E-16, 4.000000000000000000 ) ) ;
#8318=ORIENTED_EDGE ( 'NONE', *, *, #4079, .T. ) ;
#8354=VECTOR ( 'NONE', #3634, 1000.000000000000000 ) ;
#8366=EDGE_CURVE ( 'NONE', #9059, #18970, #10288, .T. ) ;
#8384=VERTEX_POINT ( 'NONE', #15715 ) ;
#8399=DIRECTION ( 'NONE',  ( 0.000000000000000000, 1.224646799147358384E-16, 1.000000000000000000 ) ) ;
#8400=AXIS2_PLACEMENT_3D ( 'NONE', #641, #11442, #6716 ) ;
#8408=ORIENTED_EDGE ( 'NONE', *, *, #9103, .T. ) ;
#8411=AXIS2_PLACEMENT_3D ( 'NONE', #7535, #11758, #14862 ) ;
#8463=DIRECTION ( 'NONE',  ( 0.000000000000000000, 0.000000000000000000, -1.000000000000000000 ) ) ;
#8483=AXIS2_PLACEMENT_3D ( 'NONE', #13137, #3933, #10052 ) ;
#8496=FILL_AREA_STYLE ('',( #10001 ) ) ;
#8512=PRESENTATION_STYLE_ASSIGNMENT (( #4001 ) ) ;
#8521=CARTESIAN_POINT ( 'NONE',  ( -0.2436698586202288019, 0.000000000000000000, 7.174999999999998934 ) ) ;
#8566=ORIENTED_EDGE ( 'NONE', *, *, #16277, .F. ) ;
#8570=AXIS2_PLACEMENT_3D ( 'NONE', #158, #17068, #12462 ) ;
#8587=ADVANCED_FACE ( 'NONE', ( #18201 ), #11997, .T. ) ;
#8589=DIRECTION ( 'NONE',  ( 1.000000000000000000, 0.000000000000000000, 0.000000000000000000 ) ) ;
#8649=VECTOR ( 'NONE', #7775, 1000.000000000000000 ) ;
#8688=AXIS2_PLACEMENT_3D ( 'NONE', #14214, #18809, #517 ) ;
#8690=EDGE_CURVE ( 'NONE', #5418, #12054, #6123, .T. ) ;
#8711=VERTEX_POINT ( 'NONE', #13693 ) ;
#8776=COLOUR_RGB ( '', 0.31764706, 0.68627451, 0.89019608) ;
#8783=DIRECTION ( 'NONE',  ( 1.000000000000000000, 0.000000000000000000, 0.000000000000000000 ) ) ;
#8884=SHAPE_REPRESENTATION_RELATIONSHIP ( 'NONE' , 'NONE' ,  #17568, #4233 ) ;
#8930=CARTESIAN_POINT ( 'NONE',  ( -2.000000000000000888, 5.143516556418882928E-16, 4.200000000000000178 ) ) ;
#8997=ORIENTED_EDGE ( 'NONE', *, *, #16277, .T. ) ;
#9059=VERTEX_POINT ( 'NONE', #10769 ) ;
#9103=EDGE_CURVE ( 'NONE', #3073, #13634, #17024, .T. ) ;
#9163=VERTEX_POINT ( 'NONE', #1953 ) ;
#9229=CARTESIAN_POINT ( 'NONE',  ( 0.000000000000000000, 0.000000000000000000, 0.000000000000000000 ) ) ;
#9277=CIRCLE ( 'NONE', #18236, 4.000000000000000000 ) ;
#9281=FACE_OUTER_BOUND ( 'NONE', #2273, .T. ) ;
#9351=DIRECTION ( 'NONE',  ( -0.000000000000000000, 1.000000000000000000, 1.224646799147353207E-16 ) ) ;
#9413=AXIS2_PLACEMENT_3D ( 'NONE', #11051, #15363, #1648 ) ;
#9431=MANIFOLD_SOLID_BREP ( 'OuterRace', #5237 ) ;
#9458=AXIS2_PLACEMENT_3D ( 'NONE', #6411, #12741, #11142 ) ;
#9503=CARTESIAN_POINT ( 'NONE',  ( -20.63749999999999574, 0.000000000000000000, 0.000000000000000000 ) ) ;
#9511=DIRECTION ( 'NONE',  ( 1.000000000000000000, 0.000000000000000000, 0.000000000000000000 ) ) ;
#9524=ORIENTED_EDGE ( 'NONE', *, *, #7599, .T. ) ;
#9543=AXIS2_PLACEMENT_3D ( 'NONE', #15194, #13591, #1583 ) ;
#9563=EDGE_LOOP ( 'NONE', ( #1480, #14156, #13619, #7902 ) ) ;
#9582=ADVANCED_FACE ( 'NONE', ( #1197 ), #17806, .T. ) ;
#9600=FACE_OUTER_BOUND ( 'NONE', #3240, .T. ) ;
#9654=EDGE_LOOP ( 'NONE', ( #13260, #8234 ) ) ;
#9674=TOROIDAL_SURFACE ( 'NONE', #17007, 6.000000000000000000, 1.199999999999999956 ) ;
#9692=CIRCLE ( 'NONE', #15755, 4.824999999999999289 ) ;
#9733=EDGE_LOOP ( 'NONE', ( #4948, #4421 ) ) ;
#9813=CARTESIAN_POINT ( 'NONE',  ( -20.63749999999999929, 0.000000000000000000, -5.200000000000000178 ) ) ;
#9833=DIRECTION ( 'NONE',  ( 0.000000000000000000, 0.000000000000000000, 1.000000000000000000 ) ) ;
#9835=LINE ( 'NONE', #4921, #1429 ) ;
#9912=ORIENTED_EDGE ( 'NONE', *, *, #5392, .T. ) ;
#9921=EDGE_CURVE ( 'NONE', #18135, #17337, #11777, .T. ) ;
#10001=FILL_AREA_STYLE_COLOUR ( '', #4918 ) ;
#10010=PRODUCT_DEFINITION_CONTEXT ( 'detailed design', #884, 'design' ) ;
#10052=DIRECTION ( 'NONE',  ( 0.000000000000000000, 0.000000000000000000, -1.000000000000000000 ) ) ;
#10128=AXIS2_PLACEMENT_3D ( 'NONE', #16998, #282, #187 ) ;
#10186=CARTESIAN_POINT ( 'NONE',  ( 0.000000000000000000, 7.347880794884119736E-16, -6.000000000000000000 ) ) ;
#10279=CARTESIAN_POINT ( 'NONE',  ( -1.800000000000000044, 0.000000000000000000, -7.800000000000000711 ) ) ;
#10288=CIRCLE ( 'NONE', #8688, 4.824999999999999289 ) ;
#10296=VECTOR ( 'NONE', #5374, 1000.000000000000000 ) ;
#10299=CARTESIAN_POINT ( 'NONE',  ( -1.799999999999999600, 0.000000000000000000, 0.000000000000000000 ) ) ;
#10315=CARTESIAN_POINT ( 'NONE',  ( -1.800000000000000488, 0.000000000000000000, 0.000000000000000000 ) ) ;
#10376=CARTESIAN_POINT ( 'NONE',  ( 1.999999999999999112, 5.143516556418882928E-16, 4.200000000000000178 ) ) ;
#10385=CARTESIAN_POINT ( 'NONE',  ( -20.63749999999999574, 9.797174393178825657E-16, 8.000000000000000000 ) ) ;
#10391=DIRECTION ( 'NONE',  ( 0.000000000000000000, 0.000000000000000000, -1.000000000000000000 ) ) ;
#10413=ORIENTED_EDGE ( 'NONE', *, *, #6129, .T. ) ;
#10426=ORIENTED_EDGE ( 'NONE', *, *, #1255, .T. ) ;
#10458=DIRECTION ( 'NONE',  ( 0.000000000000000000, -1.224646799147353207E-16, 1.000000000000000000 ) ) ;
#10482=EDGE_LOOP ( 'NONE', ( #5620, #19118 ) ) ;
#10529=CARTESIAN_POINT ( 'NONE',  ( -1.799999999999999600, 0.000000000000000000, -8.000000000000000000 ) ) ;
#10586=DIRECTION ( 'NONE',  ( 1.000000000000000000, 0.000000000000000000, 0.000000000000000000 ) ) ;
#10627=CIRCLE ( 'NONE', #1997, 6.799999999999998934 ) ;
#10641=CIRCLE ( 'NONE', #17666, 7.800000000000000711 ) ;
#10649=DIRECTION ( 'NONE',  ( 0.000000000000000000, 0.000000000000000000, -1.000000000000000000 ) ) ;
#10655=EDGE_CURVE ( 'NONE', #1107, #6633, #5931, .T. ) ;
#10672=ORIENTED_EDGE ( 'NONE', *, *, #17243, .F. ) ;
#10687=ORIENTED_EDGE ( 'NONE', *, *, #3282, .T. ) ;
#10690=EDGE_CURVE ( 'NONE', #6978, #18537, #1164, .T. ) ;
#10711=ORIENTED_EDGE ( 'NONE', *, *, #19608, .T. ) ;
#10752=CARTESIAN_POINT ( 'NONE',  ( 0.000000000000000000, 7.347880794884119736E-16, -6.000000000000000000 ) ) ;
#10753=ORIENTED_EDGE ( 'NONE', *, *, #13238, .F. ) ;
#10769=CARTESIAN_POINT ( 'NONE',  ( 2.000000000000001776, 5.908920805885978590E-16, 4.824999999999999289 ) ) ;
#10772=AXIS2_PLACEMENT_3D ( 'NONE', #2622, #5624, #11738 ) ;
#10815=ADVANCED_FACE ( 'NONE', ( #11220 ), #18723, .T. ) ;
#10825=EDGE_LOOP ( 'NONE', ( #3668, #926 ) ) ;
#10845=AXIS2_PLACEMENT_3D ( 'NONE', #18567, #17267, #1767 ) ;
#10874=ORIENTED_EDGE ( 'NONE', *, *, #8690, .F. ) ;
#10920=AXIS2_PLACEMENT_3D ( 'NONE', #18099, #4389, #2879 ) ;
#10934=DIRECTION ( 'NONE',  ( 0.000000000000000000, 0.000000000000000000, 1.000000000000000000 ) ) ;
#10946=CARTESIAN_POINT ( 'NONE',  ( -2.000000000000001776, 0.000000000000000000, 0.000000000000000000 ) ) ;
#10956=ORIENTED_EDGE ( 'NONE', *, *, #197, .T. ) ;
#10966=ORIENTED_EDGE ( 'NONE', *, *, #17243, .T. ) ;
#11049=AXIS2_PLACEMENT_3D ( 'NONE', #10279, #14975, #1367 ) ;
#11051=CARTESIAN_POINT ( 'NONE',  ( 2.000000000000001776, 0.000000000000000000, 0.000000000000000000 ) ) ;
#11067=ORIENTED_EDGE ( 'NONE', *, *, #15941, .F. ) ;
#11103=CARTESIAN_POINT ( 'NONE',  ( -2.000000000000000444, 5.200000000000000178, 0.000000000000000000 ) ) ;
#11105=CIRCLE ( 'NONE', #3114, 5.200000000000000178 ) ;
#11142=DIRECTION ( 'NONE',  ( 0.000000000000000000, 0.000000000000000000, -1.000000000000000000 ) ) ;
#11163=CARTESIAN_POINT ( 'NONE',  ( 1.800000000000000488, 0.000000000000000000, -4.200000000000000178 ) ) ;
#11190=DIRECTION ( 'NONE',  ( 1.000000000000000000, 0.000000000000000000, 0.000000000000000000 ) ) ;
#11210=AXIS2_PLACEMENT_3D ( 'NONE', #599, #1991, #6776 ) ;
#11220=FACE_OUTER_BOUND ( 'NONE', #12878, .T. ) ;
#11222=DIRECTION ( 'NONE',  ( 1.000000000000000000, 0.000000000000000000, 0.000000000000000000 ) ) ;
#11238=AXIS2_PLACEMENT_3D ( 'NONE', #14081, #12193, #2983 ) ;
#11297=DIRECTION ( 'NONE',  ( 0.000000000000000000, 1.000000000000000000, -1.224646799147353207E-16 ) ) ;
#11330=CARTESIAN_POINT ( 'NONE',  ( 0.2436698586202201144, 7.118259520043989361E-16, -4.824999999999999289 ) ) ;
#11383=CARTESIAN_POINT ( 'NONE',  ( -2.000000000000001776, 0.000000000000000000, 0.000000000000000000 ) ) ;
#11439=CARTESIAN_POINT ( 'NONE',  ( -0.2436698586202288019, 8.786840783882257924E-16, -7.174999999999998934 ) ) ;
#11442=DIRECTION ( 'NONE',  ( 1.000000000000000000, 0.000000000000000000, 0.000000000000000000 ) ) ;
#11452=CIRCLE ( 'NONE', #7921, 8.000000000000000000 ) ;
#11459=VERTEX_POINT ( 'NONE', #19380 ) ;
#11465=PRODUCT_DEFINITION_SHAPE ( 'NONE', 'NONE',  #396 ) ;
#11487=APPLICATION_CONTEXT ( 'automotive_design' ) ;
#11606=AXIS2_PLACEMENT_3D ( 'NONE', #9229, #13625, #18040 ) ;
#11640=DIRECTION ( 'NONE',  ( 1.000000000000000000, 0.000000000000000000, 0.000000000000000000 ) ) ;
#11692=EDGE_CURVE ( 'NONE', #3073, #17337, #16207, .T. ) ;
#11700=ADVANCED_FACE ( 'NONE', ( #4039 ), #576, .T. ) ;
#11723=DIRECTION ( 'NONE',  ( -1.000000000000000000, -0.000000000000000000, -0.000000000000000000 ) ) ;
#11738=DIRECTION ( 'NONE',  ( 0.000000000000000000, 0.000000000000000000, -1.000000000000000000 ) ) ;
#11758=DIRECTION ( 'NONE',  ( 1.000000000000000000, 0.000000000000000000, 0.000000000000000000 ) ) ;
#11777=LINE ( 'NONE', #10385, #1137 ) ;
#11789=CARTESIAN_POINT ( 'NONE',  ( 1.999999999999999112, 0.000000000000000000, -4.200000000000000178 ) ) ;
#11845=AXIS2_PLACEMENT_3D ( 'NONE', #13018, #815, #17612 ) ;
#11879=LINE ( 'NONE', #7353, #16429 ) ;
#11882=FACE_OUTER_BOUND ( 'NONE', #9654, .T. ) ;
#11910=EDGE_CURVE ( 'NONE', #9163, #1573, #16219, .T. ) ;
#11925=CIRCLE ( 'NONE', #15126, 0.1999999999999996503 ) ;
#11927=DIRECTION ( 'NONE',  ( 0.000000000000000000, -1.000000000000000000, 0.000000000000000000 ) ) ;
#11945=ORIENTED_EDGE ( 'NONE', *, *, #6979, .T. ) ;
#11964=VERTEX_POINT ( 'NONE', #2118 ) ;
#11983=ORIENTED_EDGE ( 'NONE', *, *, #12944, .T. ) ;
#11997=CYLINDRICAL_SURFACE ( 'NONE', #10920, 8.000000000000000000 ) ;
#12034=DIRECTION ( 'NONE',  ( 0.000000000000000000, 0.000000000000000000, -1.000000000000000000 ) ) ;
#12054=VERTEX_POINT ( 'NONE', #8521 ) ;
#12061=ORIENTED_EDGE ( 'NONE', *, *, #15186, .T. ) ;
#12067=AXIS2_PLACEMENT_3D ( 'NONE', #7217, #1238, #8463 ) ;
#12088=FACE_BOUND ( 'NONE', #17314, .T. ) ;
#12095=DIRECTION ( 'NONE',  ( 1.000000000000000000, 0.000000000000000000, 0.000000000000000000 ) ) ;
#12129=FACE_OUTER_BOUND ( 'NONE', #1823, .T. ) ;
#12193=DIRECTION ( 'NONE',  ( -1.000000000000000000, -0.000000000000000000, -0.000000000000000000 ) ) ;
#12298=DIRECTION ( 'NONE',  ( 0.000000000000000000, 0.000000000000000000, -1.000000000000000000 ) ) ;
#12349=EDGE_CURVE ( 'NONE', #18565, #2110, #7284, .T. ) ;
#12352=CIRCLE ( 'NONE', #4053, 7.800000000000000711 ) ;
#12391=CARTESIAN_POINT ( 'NONE',  ( -2.000000000000001776, 0.000000000000000000, 0.000000000000000000 ) ) ;
#12398=VERTEX_POINT ( 'NONE', #17205 ) ;
#12401=EDGE_CURVE ( 'NONE', #639, #18135, #11452, .T. ) ;
#12402=CARTESIAN_POINT ( 'NONE',  ( -20.63749999999999574, 8.327598234201999146E-16, 6.799999999999998046 ) ) ;
#12450=AXIS2_PLACEMENT_3D ( 'NONE', #7119, #17557, #4042 ) ;
#12455=EDGE_LOOP ( 'NONE', ( #5122, #8997, #11945, #1600 ) ) ;
#12462=DIRECTION ( 'NONE',  ( 0.000000000000000000, 0.000000000000000000, -1.000000000000000000 ) ) ;
#12468=DIRECTION ( 'NONE',  ( 0.000000000000000000, 0.000000000000000000, -1.000000000000000000 ) ) ;
#12484=CARTESIAN_POINT ( 'NONE',  ( -20.63749999999999929, 0.000000000000000000, -4.000000000000000000 ) ) ;
#12488=EDGE_LOOP ( 'NONE', ( #9524, #3473, #14456, #876 ) ) ;
#12509=ADVANCED_FACE ( 'NONE', ( #19092 ), #3886, .T. ) ;
#12544=CIRCLE ( 'NONE', #13181, 7.800000000000000711 ) ;
#12612=PLANE ( 'NONE',  #1390 ) ;
#12693=LINE ( 'NONE', #12402, #17918 ) ;
#12703=DIRECTION ( 'NONE',  ( 0.000000000000000000, 0.000000000000000000, -1.000000000000000000 ) ) ;
#12741=DIRECTION ( 'NONE',  ( 1.000000000000000000, 0.000000000000000000, 0.000000000000000000 ) ) ;
#12754=FACE_OUTER_BOUND ( 'NONE', #12488, .T. ) ;
#12768=VERTEX_POINT ( 'NONE', #11789 ) ;
#12800=DIRECTION ( 'NONE',  ( 0.000000000000000000, 0.000000000000000000, -1.000000000000000000 ) ) ;
#12878=EDGE_LOOP ( 'NONE', ( #18659, #10966, #6448, #13459 ) ) ;
#12912=CARTESIAN_POINT ( 'NONE',  ( 2.000000000000001776, 0.000000000000000000, 0.000000000000000000 ) ) ;
#12918=CARTESIAN_POINT ( 'NONE',  ( 0.8944271909999177428, 0.000000000000000000, 0.000000000000000000 ) ) ;
#12944=EDGE_CURVE ( 'NONE', #6633, #1107, #13687, .T. ) ;
#12968=ORIENTED_EDGE ( 'NONE', *, *, #4935, .F. ) ;
#12978=DIRECTION ( 'NONE',  ( 1.000000000000000000, 0.000000000000000000, 0.000000000000000000 ) ) ;
#13003=FACE_OUTER_BOUND ( 'NONE', #18354, .T. ) ;
#13018=CARTESIAN_POINT ( 'NONE',  ( -2.000000000000000000, 7.174999999999999822, 0.000000000000000000 ) ) ;
#13026=DIRECTION ( 'NONE',  ( 1.000000000000000000, 0.000000000000000000, 0.000000000000000000 ) ) ;
#13068=VERTEX_POINT ( 'NONE', #10376 ) ;
#13085=CARTESIAN_POINT ( 'NONE',  ( -1.800000000000000044, 9.552245033349356544E-16, 7.800000000000000711 ) ) ;
#13137=CARTESIAN_POINT ( 'NONE',  ( -20.63749999999999574, 0.000000000000000000, 0.000000000000000000 ) ) ;
#13181=AXIS2_PLACEMENT_3D ( 'NONE', #12391, #12095, #1582 ) ;
#13189=DIRECTION ( 'NONE',  ( 0.000000000000000000, 1.224646799147358384E-16, 1.000000000000000000 ) ) ;
#13238=EDGE_CURVE ( 'NONE', #4447, #16213, #6003, .T. ) ;
#13243=AXIS2_PLACEMENT_3D ( 'NONE', #13085, #11297, #13189 ) ;
#13255=CIRCLE ( 'NONE', #9413, 6.799999999999998934 ) ;
#13260=ORIENTED_EDGE ( 'NONE', *, *, #6080, .T. ) ;
#13269=ORIENTED_EDGE ( 'NONE', *, *, #2834, .F. ) ;
#13282=FACE_OUTER_BOUND ( 'NONE', #8112, .T. ) ;
#13289=DIRECTION ( 'NONE',  ( 1.000000000000000000, 0.000000000000000000, 0.000000000000000000 ) ) ;
#13335=ORIENTED_EDGE ( 'NONE', *, *, #14969, .F. ) ;
#13374=DIRECTION ( 'NONE',  ( 1.000000000000000000, 0.000000000000000000, 0.000000000000000000 ) ) ;
#13385=UNCERTAINTY_MEASURE_WITH_UNIT (LENGTH_MEASURE( 1.000000000000000082E-05 ), #3786, 'distance_accuracy_value', 'NONE');
#13438=DIRECTION ( 'NONE',  ( 0.000000000000000000, 0.000000000000000000, -1.000000000000000000 ) ) ;
#13459=ORIENTED_EDGE ( 'NONE', *, *, #4079, .F. ) ;
#13477=PRESENTATION_STYLE_ASSIGNMENT (( #1478 ) ) ;
#13493=DIRECTION ( 'NONE',  ( 0.000000000000000000, 0.000000000000000000, -1.000000000000000000 ) ) ;
#13502=AXIS2_PLACEMENT_3D ( 'NONE', #10752, #9351, #10458 ) ;
#13508=CARTESIAN_POINT ( 'NONE',  ( -20.63749999999999574, 0.000000000000000000, -6.799999999999998046 ) ) ;
#13591=DIRECTION ( 'NONE',  ( 1.000000000000000000, 0.000000000000000000, 0.000000000000000000 ) ) ;
#13619=ORIENTED_EDGE ( 'NONE', *, *, #19413, .T. ) ;
#13625=DIRECTION ( 'NONE',  ( -1.000000000000000000, -0.000000000000000000, -0.000000000000000000 ) ) ;
#13634=VERTEX_POINT ( 'NONE', #8097 ) ;
#13682=( NAMED_UNIT ( * ) PLANE_ANGLE_UNIT ( ) SI_UNIT ( $, .RADIAN. ) );
#13687=CIRCLE ( 'NONE', #7605, 4.000000000000000000 ) ;
#13693=CARTESIAN_POINT ( 'NONE',  ( 2.000000000000001776, 9.674709713264090115E-16, 7.800000000000000711 ) ) ;
#13729=VERTEX_POINT ( 'NONE', #6120 ) ;
#13743=CARTESIAN_POINT ( 'NONE',  ( -2.000000000000001776, 0.000000000000000000, 0.000000000000000000 ) ) ;
#13781=CARTESIAN_POINT ( 'NONE',  ( 2.000000000000000000, 7.800000000000000711, 0.000000000000000000 ) ) ;
#13792=DIRECTION ( 'NONE',  ( 1.000000000000000000, 0.000000000000000000, 0.000000000000000000 ) ) ;
#13826=CARTESIAN_POINT ( 'NONE',  ( 0.000000000000000000, 0.000000000000000000, 6.000000000000000000 ) ) ;
#13841=TOROIDAL_SURFACE ( 'NONE', #8400, 7.800000000000000711, 0.1999999999999998723 ) ;
#13858=CARTESIAN_POINT ( 'NONE',  ( -1.800000000000000044, 0.000000000000000000, 0.000000000000000000 ) ) ;
#13866=ADVANCED_FACE ( 'NONE', ( #8053 ), #18867, .F. ) ;
#13880=ORIENTED_EDGE ( 'NONE', *, *, #10690, .T. ) ;
#13942=FACE_OUTER_BOUND ( 'NONE', #17252, .T. ) ;
#14019=EDGE_LOOP ( 'NONE', ( #15685, #3061, #17328, #14118 ) ) ;
#14021=CARTESIAN_POINT ( 'NONE',  ( -2.000000000000001776, 6.368163355566236381E-16, 5.200000000000000178 ) ) ;
#14038=DIRECTION ( 'NONE',  ( 1.000000000000000000, 0.000000000000000000, 0.000000000000000000 ) ) ;
#14081=CARTESIAN_POINT ( 'NONE',  ( -0.2436698586202288019, 0.000000000000000000, 0.000000000000000000 ) ) ;
#14082=FACE_OUTER_BOUND ( 'NONE', #16579, .T. ) ;
#14099=CIRCLE ( 'NONE', #2576, 7.174999999999999822 ) ;
#14118=ORIENTED_EDGE ( 'NONE', *, *, #6129, .F. ) ;
#14119=DIRECTION ( 'NONE',  ( 0.000000000000000000, 0.000000000000000000, -1.000000000000000000 ) ) ;
#14149=ORIENTED_EDGE ( 'NONE', *, *, #9103, .F. ) ;
#14156=ORIENTED_EDGE ( 'NONE', *, *, #5489, .T. ) ;
#14192=DIRECTION ( 'NONE',  ( 1.000000000000000000, 0.000000000000000000, 0.000000000000000000 ) ) ;
#14214=CARTESIAN_POINT ( 'NONE',  ( 2.000000000000001776, 0.000000000000000000, 0.000000000000000000 ) ) ;
#14217=ADVANCED_FACE ( 'NONE', ( #6921 ), #2234, .F. ) ;
#14255=EDGE_LOOP ( 'NONE', ( #2453, #19042 ) ) ;
#14265=AXIS2_PLACEMENT_3D ( 'NONE', #2512, #11723, #5706 ) ;
#14302=LINE ( 'NONE', #9813, #4255 ) ;
#14336=ORIENTED_EDGE ( 'NONE', *, *, #11692, .F. ) ;
#14358=EDGE_LOOP ( 'NONE', ( #352, #3542, #6702, #1035 ) ) ;
#14411=AXIS2_PLACEMENT_3D ( 'NONE', #7428, #17858, #41 ) ;
#14419=CARTESIAN_POINT ( 'NONE',  ( 1.999999999999998224, 0.000000000000000000, 0.000000000000000000 ) ) ;
#14422=ORIENTED_EDGE ( 'NONE', *, *, #18069, .T. ) ;
#14446=DIRECTION ( 'NONE',  ( 1.000000000000000000, 0.000000000000000000, 0.000000000000000000 ) ) ;
#14448=ORIENTED_EDGE ( 'NONE', *, *, #2834, .T. ) ;
#14455=AXIS2_PLACEMENT_3D ( 'NONE', #10186, #16287, #2564 ) ;
#14456=ORIENTED_EDGE ( 'NONE', *, *, #12401, .F. ) ;
#14462=ORIENTED_EDGE ( 'NONE', *, *, #19413, .F. ) ;
#14472=AXIS2_PLACEMENT_3D ( 'NONE', #6443, #3162, #17268 ) ;
#14485=ADVANCED_FACE ( 'NONE', ( #13282 ), #3964, .T. ) ;
#14522=( NAMED_UNIT ( * ) SI_UNIT ( $, .STERADIAN. ) SOLID_ANGLE_UNIT ( ) );
#14525=DIRECTION ( 'NONE',  ( 0.000000000000000000, 0.000000000000000000, -1.000000000000000000 ) ) ;
#14563=EDGE_LOOP ( 'NONE', ( #1715, #18227, #9912, #14462 ) ) ;
#14587=DIRECTION ( 'NONE',  ( 0.000000000000000000, 0.000000000000000000, -1.000000000000000000 ) ) ;
#14634=EDGE_CURVE ( 'NONE', #11459, #7744, #3652, .T. ) ;
#14675=ORIENTED_EDGE ( 'NONE', *, *, #3216, .F. ) ;
#14747=DIRECTION ( 'NONE',  ( 0.000000000000000000, 1.000000000000000000, -1.224646799147353207E-16 ) ) ;
#14810=FACE_OUTER_BOUND ( 'NONE', #7257, .T. ) ;
#14830=VECTOR ( 'NONE', #18949, 1000.000000000000000 ) ;
#14845=DIRECTION ( 'NONE',  ( 0.000000000000000000, 1.224646799147353454E-16, 1.000000000000000000 ) ) ;
#14847=CARTESIAN_POINT ( 'NONE',  ( 1.799999999999999600, 0.000000000000000000, -4.000000000000000000 ) ) ;
#14862=DIRECTION ( 'NONE',  ( 0.000000000000000000, 0.000000000000000000, -1.000000000000000000 ) ) ;
#14876=CIRCLE ( 'NONE', #14265, 4.824999999999999289 ) ;
#14953=VERTEX_POINT ( 'NONE', #1552 ) ;
#14969=EDGE_CURVE ( 'NONE', #17016, #2110, #13255, .T. ) ;
#14975=DIRECTION ( 'NONE',  ( 0.000000000000000000, -1.000000000000000000, 0.000000000000000000 ) ) ;
#14989=ADVANCED_FACE ( 'NONE', ( #12754 ), #7796, .T. ) ;
#15011=CARTESIAN_POINT ( 'NONE',  ( 1.999999999999998224, 0.000000000000000000, 0.000000000000000000 ) ) ;
#15033=DIRECTION ( 'NONE',  ( 1.000000000000000000, 0.000000000000000000, 0.000000000000000000 ) ) ;
#15126=AXIS2_PLACEMENT_3D ( 'NONE', #2858, #14747, #14845 ) ;
#15151=CIRCLE ( 'NONE', #13243, 0.1999999999999996503 ) ;
#15174=CARTESIAN_POINT ( 'NONE',  ( 1.800000000000000044, 0.000000000000000000, -7.800000000000000711 ) ) ;
#15186=EDGE_CURVE ( 'NONE', #18537, #4447, #17742, .T. ) ;
#15194=CARTESIAN_POINT ( 'NONE',  ( 2.000000000000001776, 0.000000000000000000, 0.000000000000000000 ) ) ;
#15328=AXIS2_PLACEMENT_3D ( 'NONE', #2343, #851, #5438 ) ;
#15338=FACE_BOUND ( 'NONE', #10825, .T. ) ;
#15362=ORIENTED_EDGE ( 'NONE', *, *, #1733, .F. ) ;
#15363=DIRECTION ( 'NONE',  ( 1.000000000000000000, 0.000000000000000000, 0.000000000000000000 ) ) ;
#15390=LINE ( 'NONE', #12484, #8649 ) ;
#15411=DIRECTION ( 'NONE',  ( 1.000000000000000000, 0.000000000000000000, 0.000000000000000000 ) ) ;
#15424=ORIENTED_EDGE ( 'NONE', *, *, #3216, .T. ) ;
#15437=DIRECTION ( 'NONE',  ( 1.000000000000000000, 0.000000000000000000, 0.000000000000000000 ) ) ;
#15438=TOROIDAL_SURFACE ( 'NONE', #17038, 6.000000000000000000, 1.199999999999999956 ) ;
#15453=FACE_OUTER_BOUND ( 'NONE', #16248, .T. ) ;
#15492=( GEOMETRIC_REPRESENTATION_CONTEXT ( 3 ) GLOBAL_UNCERTAINTY_ASSIGNED_CONTEXT ( ( #7361 ) ) GLOBAL_UNIT_ASSIGNED_CONTEXT ( ( #2300, #17708, #14522 ) ) REPRESENTATION_CONTEXT ( 'NONE', 'WORKASPACE' ) );
#15504=DIRECTION ( 'NONE',  ( 0.000000000000000000, 0.000000000000000000, -1.000000000000000000 ) ) ;
#15523=ORIENTED_EDGE ( 'NONE', *, *, #15186, .F. ) ;
#15538=ORIENTED_EDGE ( 'NONE', *, *, #8690, .T. ) ;
#15552=ORIENTED_EDGE ( 'NONE', *, *, #17641, .T. ) ;
#15570=DIRECTION ( 'NONE',  ( 0.000000000000000000, -1.000000000000000000, 0.000000000000000000 ) ) ;
#15657=PRODUCT_CONTEXT ( 'NONE', #11487, 'mechanical' ) ;
#15685=ORIENTED_EDGE ( 'NONE', *, *, #14634, .T. ) ;
#15688=CIRCLE ( 'NONE', #14411, 0.1999999999999996503 ) ;
#15691=EDGE_CURVE ( 'NONE', #2239, #12398, #5431, .T. ) ;
#15704=DIRECTION ( 'NONE',  ( -0.000000000000000000, 0.000000000000000000, 1.000000000000000000 ) ) ;
#15715=CARTESIAN_POINT ( 'NONE',  ( -2.000000000000001776, 0.000000000000000000, -7.800000000000000711 ) ) ;
#15726=AXIS2_PLACEMENT_3D ( 'NONE', #13781, #10586, #4475 ) ;
#15743=DIRECTION ( 'NONE',  ( 0.000000000000000000, 0.000000000000000000, 1.000000000000000000 ) ) ;
#15755=AXIS2_PLACEMENT_3D ( 'NONE', #7420, #6027, #13438 ) ;
#15804=DIRECTION ( 'NONE',  ( 1.000000000000000000, 0.000000000000000000, 0.000000000000000000 ) ) ;
#15877=ORIENTED_EDGE ( 'NONE', *, *, #13238, .T. ) ;
#15916=ORIENTED_EDGE ( 'NONE', *, *, #7599, .F. ) ;
#15941=EDGE_CURVE ( 'NONE', #11964, #19760, #5750, .T. ) ;
#16012=SURFACE_SIDE_STYLE ('',( #6691 ) ) ;
#16014=FACE_BOUND ( 'NONE', #3359, .T. ) ;
#16081=DIRECTION ( 'NONE',  ( 0.000000000000000000, 0.000000000000000000, -1.000000000000000000 ) ) ;
#16089=TOROIDAL_SURFACE ( 'NONE', #11606, 6.000000000000000000, 1.199999999999999956 ) ;
#16108=CARTESIAN_POINT ( 'NONE',  ( -20.63749999999999574, 8.786840783882257924E-16, 7.174999999999998934 ) ) ;
#16113=( GEOMETRIC_REPRESENTATION_CONTEXT ( 3 ) GLOBAL_UNCERTAINTY_ASSIGNED_CONTEXT ( ( #13385 ) ) GLOBAL_UNIT_ASSIGNED_CONTEXT ( ( #3786, #7159, #5381 ) ) REPRESENTATION_CONTEXT ( 'NONE', 'WORKASPACE' ) );
#16124=CARTESIAN_POINT ( 'NONE',  ( 1.799999999999999600, 9.797174393178825657E-16, 8.000000000000000000 ) ) ;
#16165=ORIENTED_EDGE ( 'NONE', *, *, #783, .F. ) ;
#16196=LINE ( 'NONE', #3781, #10296 ) ;
#16207=CIRCLE ( 'NONE', #17799, 8.000000000000000000 ) ;
#16211=ADVANCED_FACE ( 'NONE', ( #755 ), #7213, .F. ) ;
#16213=VERTEX_POINT ( 'NONE', #3844 ) ;
#16215=PLANE ( 'NONE',  #11845 ) ;
#16219=CIRCLE ( 'NONE', #6934, 4.200000000000000178 ) ;
#16248=EDGE_LOOP ( 'NONE', ( #14675, #10711, #8408, #12968 ) ) ;
#16277=EDGE_CURVE ( 'NONE', #18135, #639, #17566, .T. ) ;
#16287=DIRECTION ( 'NONE',  ( -0.000000000000000000, 1.000000000000000000, 1.224646799147353207E-16 ) ) ;
#16383=DIRECTION ( 'NONE',  ( 1.000000000000000000, 0.000000000000000000, 0.000000000000000000 ) ) ;
#16393=ADVANCED_FACE ( 'NONE', ( #17040 ), #1277, .T. ) ;
#16394=LINE ( 'NONE', #16108, #437 ) ;
#16410=AXIS2_PLACEMENT_3D ( 'NONE', #9503, #14192, #15504 ) ;
#16429=VECTOR ( 'NONE', #13374, 1000.000000000000000 ) ;
#16490=CARTESIAN_POINT ( 'NONE',  ( -1.799999999999999600, 0.000000000000000000, 0.000000000000000000 ) ) ;
#16520=ORIENTED_EDGE ( 'NONE', *, *, #3108, .T. ) ;
#16579=EDGE_LOOP ( 'NONE', ( #292, #3530, #206, #6209 ) ) ;
#16678=AXIS2_PLACEMENT_3D ( 'NONE', #10315, #17809, #14525 ) ;
#16717=AXIS2_PLACEMENT_3D ( 'NONE', #17893, #986, #8399 ) ;
#16724=AXIS2_PLACEMENT_3D ( 'NONE', #17428, #9833, #6230 ) ;
#16766=DIRECTION ( 'NONE',  ( 1.000000000000000000, 0.000000000000000000, 0.000000000000000000 ) ) ;
#16840=CARTESIAN_POINT ( 'NONE',  ( 2.000000000000000000, 4.200000000000000178, 0.000000000000000000 ) ) ;
#16936=CARTESIAN_POINT ( 'NONE',  ( -2.000000000000001776, 0.000000000000000000, 0.000000000000000000 ) ) ;
#16963=SHAPE_DEFINITION_REPRESENTATION ( #11465, #17568 ) ;
#16998=CARTESIAN_POINT ( 'NONE',  ( -20.63749999999999574, 0.000000000000000000, 0.000000000000000000 ) ) ;
#17007=AXIS2_PLACEMENT_3D ( 'NONE', #19299, #5590, #4006 ) ;
#17016=VERTEX_POINT ( 'NONE', #19687 ) ;
#17024=CIRCLE ( 'NONE', #19564, 0.1999999999999996503 ) ;
#17032=EDGE_CURVE ( 'NONE', #7744, #11459, #9277, .T. ) ;
#17038=AXIS2_PLACEMENT_3D ( 'NONE', #18166, #2843, #18259 ) ;
#17040=FACE_OUTER_BOUND ( 'NONE', #9563, .T. ) ;
#17047=CIRCLE ( 'NONE', #16717, 0.1999999999999996503 ) ;
#17068=DIRECTION ( 'NONE',  ( 1.000000000000000000, 0.000000000000000000, 0.000000000000000000 ) ) ;
#17075=ORIENTED_EDGE ( 'NONE', *, *, #12401, .T. ) ;
#17105=AXIS2_PLACEMENT_3D ( 'NONE', #16490, #2866, #10391 ) ;
#17142=CYLINDRICAL_SURFACE ( 'NONE', #19206, 5.200000000000000178 ) ;
#17144=EDGE_CURVE ( 'NONE', #11459, #6633, #15390, .T. ) ;
#17157=DIRECTION ( 'NONE',  ( 1.000000000000000000, 0.000000000000000000, 0.000000000000000000 ) ) ;
#17205=CARTESIAN_POINT ( 'NONE',  ( -2.000000000000001776, 0.000000000000000000, -7.174999999999999822 ) ) ;
#17206=DIRECTION ( 'NONE',  ( -1.000000000000000000, 0.000000000000000000, -0.000000000000000000 ) ) ;
#17219=ADVANCED_FACE ( 'NONE', ( #17962 ), #4162, .T. ) ;
#17238=DIRECTION ( 'NONE',  ( 0.000000000000000000, 0.000000000000000000, -1.000000000000000000 ) ) ;
#17243=EDGE_CURVE ( 'NONE', #13068, #1107, #15688, .T. ) ;
#17252=EDGE_LOOP ( 'NONE', ( #15523, #6738, #16520, #10753 ) ) ;
#17267=DIRECTION ( 'NONE',  ( 1.000000000000000000, 0.000000000000000000, 0.000000000000000000 ) ) ;
#17268=DIRECTION ( 'NONE',  ( 0.000000000000000000, 0.000000000000000000, -1.000000000000000000 ) ) ;
#17287=AXIS2_PLACEMENT_3D ( 'NONE', #14419, #4003, #17710 ) ;
#17305=CARTESIAN_POINT ( 'NONE',  ( -2.000000000000001776, 0.000000000000000000, 0.000000000000000000 ) ) ;
#17314=EDGE_LOOP ( 'NONE', ( #13269, #13335 ) ) ;
#17328=ORIENTED_EDGE ( 'NONE', *, *, #11910, .F. ) ;
#17332=CARTESIAN_POINT ( 'NONE',  ( 0.000000000000000000, 0.000000000000000000, 0.000000000000000000 ) ) ;
#17337=VERTEX_POINT ( 'NONE', #16124 ) ;
#17404=EDGE_CURVE ( 'NONE', #13068, #12768, #2562, .T. ) ;
#17428=CARTESIAN_POINT ( 'NONE',  ( 0.000000000000000000, 0.000000000000000000, 0.000000000000000000 ) ) ;
#17440=CIRCLE ( 'NONE', #182, 6.799999999999998046 ) ;
#17465=ADVANCED_FACE ( 'NONE', ( #16014, #2301 ), #16215, .T. ) ;
#17557=DIRECTION ( 'NONE',  ( 1.000000000000000000, 0.000000000000000000, 0.000000000000000000 ) ) ;
#17566=CIRCLE ( 'NONE', #15328, 8.000000000000000000 ) ;
#17568=SHAPE_REPRESENTATION ( 'angular contact ball bearing_68_iso_ISO 15 ABB - 188 - 12,SI,NC,12_68', ( #16724 ), #16113 ) ;
#17589=CARTESIAN_POINT ( 'NONE',  ( 2.000000000000001776, 0.000000000000000000, -4.824999999999999289 ) ) ;
#17598=CARTESIAN_POINT ( 'NONE',  ( -20.63749999999999574, 0.000000000000000000, 0.000000000000000000 ) ) ;
#17610=ORIENTED_EDGE ( 'NONE', *, *, #14969, .T. ) ;
#17612=DIRECTION ( 'NONE',  ( -0.000000000000000000, 0.000000000000000000, 1.000000000000000000 ) ) ;
#17615=DIRECTION ( 'NONE',  ( 0.000000000000000000, 0.000000000000000000, 1.000000000000000000 ) ) ;
#17634=TOROIDAL_SURFACE ( 'NONE', #16678, 4.200000000000000178, 0.1999999999999998723 ) ;
#17641=EDGE_CURVE ( 'NONE', #14953, #17016, #12693, .T. ) ;
#17666=AXIS2_PLACEMENT_3D ( 'NONE', #13743, #18057, #10649 ) ;
#17677=DIRECTION ( 'NONE',  ( 0.000000000000000000, 0.000000000000000000, -1.000000000000000000 ) ) ;
#17688=DIRECTION ( 'NONE',  ( 0.000000000000000000, 0.000000000000000000, -1.000000000000000000 ) ) ;
#17708=( NAMED_UNIT ( * ) PLANE_ANGLE_UNIT ( ) SI_UNIT ( $, .RADIAN. ) );
#17710=DIRECTION ( 'NONE',  ( 0.000000000000000000, 0.000000000000000000, -1.000000000000000000 ) ) ;
#17713=ORIENTED_EDGE ( 'NONE', *, *, #17996, .T. ) ;
#17726=CARTESIAN_POINT ( 'NONE',  ( -2.000000000000001776, 0.000000000000000000, -5.200000000000000178 ) ) ;
#17742=LINE ( 'NONE', #2338, #14830 ) ;
#17785=AXIS2_PLACEMENT_3D ( 'NONE', #18299, #4687, #12298 ) ;
#17794=DIRECTION ( 'NONE',  ( 1.000000000000000000, 0.000000000000000000, 0.000000000000000000 ) ) ;
#17799=AXIS2_PLACEMENT_3D ( 'NONE', #19333, #11640, #4969 ) ;
#17806=CYLINDRICAL_SURFACE ( 'NONE', #2707, 5.200000000000000178 ) ;
#17809=DIRECTION ( 'NONE',  ( 1.000000000000000000, 0.000000000000000000, 0.000000000000000000 ) ) ;
#17823=CARTESIAN_POINT ( 'NONE',  ( -20.63749999999999574, 0.000000000000000000, -8.000000000000000000 ) ) ;
#17838=ORIENTED_EDGE ( 'NONE', *, *, #531, .T. ) ;
#17858=DIRECTION ( 'NONE',  ( 0.000000000000000000, 1.000000000000000000, -1.224646799147353207E-16 ) ) ;
#17893=CARTESIAN_POINT ( 'NONE',  ( 1.800000000000000044, 9.552245033349356544E-16, 7.800000000000000711 ) ) ;
#17918=VECTOR ( 'NONE', #11190, 1000.000000000000000 ) ;
#17962=FACE_OUTER_BOUND ( 'NONE', #18854, .T. ) ;
#17991=CIRCLE ( 'NONE', #8411, 8.000000000000000000 ) ;
#17995=ORIENTED_EDGE ( 'NONE', *, *, #9921, .T. ) ;
#17996=EDGE_CURVE ( 'NONE', #12398, #2239, #14099, .T. ) ;
#18034=AXIS2_PLACEMENT_3D ( 'NONE', #3878, #5283, #17688 ) ;
#18040=DIRECTION ( 'NONE',  ( 0.000000000000000000, 0.000000000000000000, 1.000000000000000000 ) ) ;
#18057=DIRECTION ( 'NONE',  ( 1.000000000000000000, 0.000000000000000000, 0.000000000000000000 ) ) ;
#18069=EDGE_CURVE ( 'NONE', #11964, #9059, #18940, .T. ) ;
#18078=CIRCLE ( 'NONE', #9458, 5.200000000000000178 ) ;
#18099=CARTESIAN_POINT ( 'NONE',  ( -20.63749999999999574, 0.000000000000000000, 0.000000000000000000 ) ) ;
#18135=VERTEX_POINT ( 'NONE', #444 ) ;
#18165=CIRCLE ( 'NONE', #9543, 7.800000000000000711 ) ;
#18166=CARTESIAN_POINT ( 'NONE',  ( 0.000000000000000000, 0.000000000000000000, 0.000000000000000000 ) ) ;
#18201=FACE_OUTER_BOUND ( 'NONE', #12455, .T. ) ;
#18227=ORIENTED_EDGE ( 'NONE', *, *, #19044, .T. ) ;
#18236=AXIS2_PLACEMENT_3D ( 'NONE', #10299, #13289, #7569 ) ;
#18257=DIRECTION ( 'NONE',  ( 0.000000000000000000, 0.000000000000000000, -1.000000000000000000 ) ) ;
#18259=DIRECTION ( 'NONE',  ( 0.000000000000000000, 0.000000000000000000, 1.000000000000000000 ) ) ;
#18288=EDGE_LOOP ( 'NONE', ( #18448, #18975, #2459, #18981 ) ) ;
#18299=CARTESIAN_POINT ( 'NONE',  ( -1.800000000000000488, 0.000000000000000000, -4.200000000000000178 ) ) ;
#18354=EDGE_LOOP ( 'NONE', ( #17075, #17995, #14336, #19652 ) ) ;
#18427=PLANE ( 'NONE',  #3018 ) ;
#18448=ORIENTED_EDGE ( 'NONE', *, *, #17032, .F. ) ;
#18518=EDGE_LOOP ( 'NONE', ( #19301, #10687, #10874, #15362 ) ) ;
#18524=DIRECTION ( 'NONE',  ( 1.000000000000000000, 0.000000000000000000, 0.000000000000000000 ) ) ;
#18537=VERTEX_POINT ( 'NONE', #14021 ) ;
#18565=VERTEX_POINT ( 'NONE', #19201 ) ;
#18567=CARTESIAN_POINT ( 'NONE',  ( -20.63749999999999929, 0.000000000000000000, 0.000000000000000000 ) ) ;
#18570=ADVANCED_FACE ( 'NONE', ( #5308 ), #17634, .T. ) ;
#18580=ADVANCED_FACE ( 'NONE', ( #14810 ), #9674, .T. ) ;
#18618=AXIS2_PLACEMENT_3D ( 'NONE', #4772, #269, #16081 ) ;
#18648=ORIENTED_EDGE ( 'NONE', *, *, #19012, .F. ) ;
#18658=DIRECTION ( 'NONE',  ( 0.000000000000000000, 0.000000000000000000, -1.000000000000000000 ) ) ;
#18659=ORIENTED_EDGE ( 'NONE', *, *, #2017, .T. ) ;
#18723=TOROIDAL_SURFACE ( 'NONE', #4032, 4.200000000000000178, 0.1999999999999998723 ) ;
#18809=DIRECTION ( 'NONE',  ( 1.000000000000000000, 0.000000000000000000, 0.000000000000000000 ) ) ;
#18818=CARTESIAN_POINT ( 'NONE',  ( 1.800000000000000488, 0.000000000000000000, 0.000000000000000000 ) ) ;
#18829=DIRECTION ( 'NONE',  ( -1.000000000000000000, -0.000000000000000000, -0.000000000000000000 ) ) ;
#18854=EDGE_LOOP ( 'NONE', ( #5273, #3269, #10413, #3091 ) ) ;
#18867=CYLINDRICAL_SURFACE ( 'NONE', #10845, 4.000000000000000000 ) ;
#18871=ORIENTED_EDGE ( 'NONE', *, *, #5392, .F. ) ;
#18909=FILL_AREA_STYLE ('',( #5400 ) ) ;
#18940=LINE ( 'NONE', #8027, #8354 ) ;
#18943=TOROIDAL_SURFACE ( 'NONE', #8067, 7.800000000000000711, 0.1999999999999998723 ) ;
#18949=DIRECTION ( 'NONE',  ( 1.000000000000000000, 0.000000000000000000, 0.000000000000000000 ) ) ;
#18970=VERTEX_POINT ( 'NONE', #17589 ) ;
#18975=ORIENTED_EDGE ( 'NONE', *, *, #1342, .T. ) ;
#18981=ORIENTED_EDGE ( 'NONE', *, *, #17144, .F. ) ;
#19012=EDGE_CURVE ( 'NONE', #19760, #18970, #16196, .T. ) ;
#19042=ORIENTED_EDGE ( 'NONE', *, *, #3919, .F. ) ;
#19044=EDGE_CURVE ( 'NONE', #19760, #18565, #715, .T. ) ;
#19092=FACE_OUTER_BOUND ( 'NONE', #7161, .T. ) ;
#19118=ORIENTED_EDGE ( 'NONE', *, *, #7862, .T. ) ;
#19170=AXIS2_PLACEMENT_3D ( 'NONE', #825, #13026, #1004 ) ;
#19182=SURFACE_SIDE_STYLE ('',( #889 ) ) ;
#19199=ADVANCED_FACE ( 'NONE', ( #1568 ), #18943, .T. ) ;
#19201=CARTESIAN_POINT ( 'NONE',  ( 0.8944271909999176318, 8.327598234201999146E-16, -6.799999999999998046 ) ) ;
#19206=AXIS2_PLACEMENT_3D ( 'NONE', #5028, #8130, #17238 ) ;
#19289=AXIS2_PLACEMENT_3D ( 'NONE', #2665, #8783, #3984 ) ;
#19299=CARTESIAN_POINT ( 'NONE',  ( 0.000000000000000000, 0.000000000000000000, 0.000000000000000000 ) ) ;
#19301=ORIENTED_EDGE ( 'NONE', *, *, #15691, .F. ) ;
#19333=CARTESIAN_POINT ( 'NONE',  ( 1.799999999999999600, 0.000000000000000000, 0.000000000000000000 ) ) ;
#19380=CARTESIAN_POINT ( 'NONE',  ( -1.799999999999999600, 0.000000000000000000, -4.000000000000000000 ) ) ;
#19413=EDGE_CURVE ( 'NONE', #11964, #14953, #2636, .T. ) ;
#19470=ORIENTED_EDGE ( 'NONE', *, *, #7884, .F. ) ;
#19564=AXIS2_PLACEMENT_3D ( 'NONE', #15174, #15570, #12468 ) ;
#19608=EDGE_CURVE ( 'NONE', #17337, #3073, #17991, .T. ) ;
#19633=ADVANCED_FACE ( 'NONE', ( #2741 ), #15438, .T. ) ;
#19652=ORIENTED_EDGE ( 'NONE', *, *, #6979, .F. ) ;
#19687=CARTESIAN_POINT ( 'NONE',  ( 2.000000000000001776, 8.327598234202001119E-16, 6.799999999999999822 ) ) ;
#19760=VERTEX_POINT ( 'NONE', #11330 ) ;
ENDSEC;
END-ISO-10303-21;
